ISO-10303-21;
HEADER;
/* Generated by software containing ST-Developer
 * from STEP Tools, Inc. (www.steptools.com) 
 */

FILE_DESCRIPTION(
/* description */ ('Crank-driven oscillating fan base (mechanism only)'),

/* implementation_level */ '2;1');

FILE_NAME(
/* name */ 'M4x10 Cap Screw.step',
/* time_stamp */ '2026-10-28T03:25:00-07:00',
/* author */ (''),
/* organization */ (''),
/* preprocessor_version */ 'ST-DEVELOPER v20.2',
/* originating_system */ 'Autodesk Translation Framework v15.17.0.0',
/* authorisation */ '');

FILE_SCHEMA (('AUTOMOTIVE_DESIGN { 1 0 10303 214 3 1 1 }'));
ENDSEC;

DATA;
#10=MECHANICAL_DESIGN_GEOMETRIC_PRESENTATION_REPRESENTATION('',(#481),#11916);
#307=CONICAL_SURFACE('',#7303,0.325,0.785398163397448);
#308=CONICAL_SURFACE('',#7307,0.335,0.785398163397448);
#309=CONICAL_SURFACE('',#7311,0.21,0.463647609000806);
#312=ORIENTED_CLOSED_SHELL('',*,#6113,.F.);
#315=BREP_WITH_VOIDS('Body1',#6114,(#312));
#393=SHAPE_REPRESENTATION_RELATIONSHIP('SRR','None',#12120,#433);
#433=ADVANCED_BREP_SHAPE_REPRESENTATION('',(#315),#11911);
#481=STYLED_ITEM('',(#12382),#315);
#683=FACE_BOUND('',#1771,.T.);
#867=PLANE('',#7291);
#868=PLANE('',#7292);
#869=PLANE('',#7293);
#870=PLANE('',#7294);
#871=PLANE('',#7295);
#872=PLANE('',#7296);
#873=PLANE('',#7297);
#874=PLANE('',#7298);
#875=PLANE('',#7299);
#876=PLANE('',#7301);
#877=PLANE('',#7309);
#1229=FACE_OUTER_BOUND('',#1757,.T.);
#1230=FACE_OUTER_BOUND('',#1758,.T.);
#1231=FACE_OUTER_BOUND('',#1759,.T.);
#1232=FACE_OUTER_BOUND('',#1760,.T.);
#1233=FACE_OUTER_BOUND('',#1761,.T.);
#1234=FACE_OUTER_BOUND('',#1762,.T.);
#1235=FACE_OUTER_BOUND('',#1763,.T.);
#1236=FACE_OUTER_BOUND('',#1764,.T.);
#1237=FACE_OUTER_BOUND('',#1765,.T.);
#1238=FACE_OUTER_BOUND('',#1766,.T.);
#1239=FACE_OUTER_BOUND('',#1767,.T.);
#1240=FACE_OUTER_BOUND('',#1768,.T.);
#1241=FACE_OUTER_BOUND('',#1769,.T.);
#1242=FACE_OUTER_BOUND('',#1770,.T.);
#1243=FACE_OUTER_BOUND('',#1772,.T.);
#1244=FACE_OUTER_BOUND('',#1773,.T.);
#1757=EDGE_LOOP('',(#5426,#5427,#5428,#5429));
#1758=EDGE_LOOP('',(#5430,#5431,#5432,#5433));
#1759=EDGE_LOOP('',(#5434,#5435,#5436,#5437));
#1760=EDGE_LOOP('',(#5438,#5439,#5440,#5441));
#1761=EDGE_LOOP('',(#5442,#5443,#5444,#5445));
#1762=EDGE_LOOP('',(#5446,#5447,#5448,#5449));
#1763=EDGE_LOOP('',(#5450,#5451,#5452,#5453,#5454,#5455));
#1764=EDGE_LOOP('',(#5456,#5457,#5458,#5459,#5460,#5461));
#1765=EDGE_LOOP('',(#5462));
#1766=EDGE_LOOP('',(#5463));
#1767=EDGE_LOOP('',(#5464,#5465,#5466,#5467));
#1768=EDGE_LOOP('',(#5468,#5469,#5470,#5471));
#1769=EDGE_LOOP('',(#5472,#5473,#5474,#5475));
#1770=EDGE_LOOP('',(#5476));
#1771=EDGE_LOOP('',(#5477));
#1772=EDGE_LOOP('',(#5478,#5479,#5480,#5481));
#1773=EDGE_LOOP('',(#5482,#5483,#5484,#5485));
#2094=LINE('',#11630,#2427);
#2095=LINE('',#11632,#2428);
#2096=LINE('',#11634,#2429);
#2097=LINE('',#11635,#2430);
#2098=LINE('',#11638,#2431);
#2099=LINE('',#11640,#2432);
#2100=LINE('',#11641,#2433);
#2101=LINE('',#11644,#2434);
#2102=LINE('',#11646,#2435);
#2103=LINE('',#11647,#2436);
#2104=LINE('',#11650,#2437);
#2105=LINE('',#11652,#2438);
#2106=LINE('',#11653,#2439);
#2107=LINE('',#11656,#2440);
#2108=LINE('',#11658,#2441);
#2109=LINE('',#11659,#2442);
#2110=LINE('',#11661,#2443);
#2111=LINE('',#11662,#2444);
#2112=LINE('',#11674,#2445);
#2113=LINE('',#11678,#2446);
#2114=LINE('',#11682,#2447);
#2115=LINE('',#11689,#2448);
#2116=LINE('',#11691,#2449);
#2427=VECTOR('',#9173,1.);
#2428=VECTOR('',#9174,1.);
#2429=VECTOR('',#9175,1.);
#2430=VECTOR('',#9176,1.);
#2431=VECTOR('',#9179,1.);
#2432=VECTOR('',#9180,1.);
#2433=VECTOR('',#9181,1.);
#2434=VECTOR('',#9184,1.);
#2435=VECTOR('',#9185,1.);
#2436=VECTOR('',#9186,1.);
#2437=VECTOR('',#9189,1.);
#2438=VECTOR('',#9190,1.);
#2439=VECTOR('',#9191,1.);
#2440=VECTOR('',#9194,1.);
#2441=VECTOR('',#9195,1.);
#2442=VECTOR('',#9196,1.);
#2443=VECTOR('',#9199,1.);
#2444=VECTOR('',#9200,1.);
#2445=VECTOR('',#9217,0.325);
#2446=VECTOR('',#9222,0.35);
#2447=VECTOR('',#9227,0.335);
#2448=VECTOR('',#9236,0.21);
#2449=VECTOR('',#9239,0.2);
#2806=CIRCLE('',#7300,0.1954);
#2807=CIRCLE('',#7302,0.3);
#2808=CIRCLE('',#7304,0.35);
#2809=CIRCLE('',#7306,0.35);
#2810=CIRCLE('',#7308,0.32);
#2811=CIRCLE('',#7310,0.22);
#2812=CIRCLE('',#7312,0.1954);
#3290=VERTEX_POINT('',#11628);
#3291=VERTEX_POINT('',#11629);
#3292=VERTEX_POINT('',#11631);
#3293=VERTEX_POINT('',#11633);
#3294=VERTEX_POINT('',#11637);
#3295=VERTEX_POINT('',#11639);
#3296=VERTEX_POINT('',#11643);
#3297=VERTEX_POINT('',#11645);
#3298=VERTEX_POINT('',#11649);
#3299=VERTEX_POINT('',#11651);
#3300=VERTEX_POINT('',#11655);
#3301=VERTEX_POINT('',#11657);
#3302=VERTEX_POINT('',#11666);
#3303=VERTEX_POINT('',#11669);
#3304=VERTEX_POINT('',#11672);
#3305=VERTEX_POINT('',#11676);
#3306=VERTEX_POINT('',#11680);
#3307=VERTEX_POINT('',#11684);
#3308=VERTEX_POINT('',#11687);
#4008=EDGE_CURVE('',#3290,#3291,#2094,.T.);
#4009=EDGE_CURVE('',#3291,#3292,#2095,.T.);
#4010=EDGE_CURVE('',#3292,#3293,#2096,.T.);
#4011=EDGE_CURVE('',#3290,#3293,#2097,.T.);
#4012=EDGE_CURVE('',#3291,#3294,#2098,.T.);
#4013=EDGE_CURVE('',#3294,#3295,#2099,.T.);
#4014=EDGE_CURVE('',#3295,#3292,#2100,.T.);
#4015=EDGE_CURVE('',#3294,#3296,#2101,.T.);
#4016=EDGE_CURVE('',#3296,#3297,#2102,.T.);
#4017=EDGE_CURVE('',#3297,#3295,#2103,.T.);
#4018=EDGE_CURVE('',#3296,#3298,#2104,.T.);
#4019=EDGE_CURVE('',#3298,#3299,#2105,.T.);
#4020=EDGE_CURVE('',#3299,#3297,#2106,.T.);
#4021=EDGE_CURVE('',#3298,#3300,#2107,.T.);
#4022=EDGE_CURVE('',#3300,#3301,#2108,.T.);
#4023=EDGE_CURVE('',#3301,#3299,#2109,.T.);
#4024=EDGE_CURVE('',#3300,#3290,#2110,.T.);
#4025=EDGE_CURVE('',#3293,#3301,#2111,.T.);
#4026=EDGE_CURVE('',#3302,#3302,#2806,.T.);
#4027=EDGE_CURVE('',#3303,#3303,#2807,.T.);
#4028=EDGE_CURVE('',#3304,#3304,#2808,.T.);
#4029=EDGE_CURVE('',#3304,#3303,#2112,.T.);
#4030=EDGE_CURVE('',#3305,#3305,#2809,.T.);
#4031=EDGE_CURVE('',#3305,#3304,#2113,.T.);
#4032=EDGE_CURVE('',#3306,#3306,#2810,.T.);
#4033=EDGE_CURVE('',#3306,#3305,#2114,.T.);
#4034=EDGE_CURVE('',#3307,#3307,#2811,.T.);
#4035=EDGE_CURVE('',#3308,#3308,#2812,.F.);
#4036=EDGE_CURVE('',#3308,#3307,#2115,.T.);
#4037=EDGE_CURVE('',#3302,#3308,#2116,.T.);
#5426=ORIENTED_EDGE('',*,*,#4008,.T.);
#5427=ORIENTED_EDGE('',*,*,#4009,.T.);
#5428=ORIENTED_EDGE('',*,*,#4010,.T.);
#5429=ORIENTED_EDGE('',*,*,#4011,.F.);
#5430=ORIENTED_EDGE('',*,*,#4012,.T.);
#5431=ORIENTED_EDGE('',*,*,#4013,.T.);
#5432=ORIENTED_EDGE('',*,*,#4014,.T.);
#5433=ORIENTED_EDGE('',*,*,#4009,.F.);
#5434=ORIENTED_EDGE('',*,*,#4015,.T.);
#5435=ORIENTED_EDGE('',*,*,#4016,.T.);
#5436=ORIENTED_EDGE('',*,*,#4017,.T.);
#5437=ORIENTED_EDGE('',*,*,#4013,.F.);
#5438=ORIENTED_EDGE('',*,*,#4018,.T.);
#5439=ORIENTED_EDGE('',*,*,#4019,.T.);
#5440=ORIENTED_EDGE('',*,*,#4020,.T.);
#5441=ORIENTED_EDGE('',*,*,#4016,.F.);
#5442=ORIENTED_EDGE('',*,*,#4021,.T.);
#5443=ORIENTED_EDGE('',*,*,#4022,.T.);
#5444=ORIENTED_EDGE('',*,*,#4023,.T.);
#5445=ORIENTED_EDGE('',*,*,#4019,.F.);
#5446=ORIENTED_EDGE('',*,*,#4024,.T.);
#5447=ORIENTED_EDGE('',*,*,#4011,.T.);
#5448=ORIENTED_EDGE('',*,*,#4025,.T.);
#5449=ORIENTED_EDGE('',*,*,#4022,.F.);
#5450=ORIENTED_EDGE('',*,*,#4024,.F.);
#5451=ORIENTED_EDGE('',*,*,#4021,.F.);
#5452=ORIENTED_EDGE('',*,*,#4018,.F.);
#5453=ORIENTED_EDGE('',*,*,#4015,.F.);
#5454=ORIENTED_EDGE('',*,*,#4012,.F.);
#5455=ORIENTED_EDGE('',*,*,#4008,.F.);
#5456=ORIENTED_EDGE('',*,*,#4025,.F.);
#5457=ORIENTED_EDGE('',*,*,#4010,.F.);
#5458=ORIENTED_EDGE('',*,*,#4014,.F.);
#5459=ORIENTED_EDGE('',*,*,#4017,.F.);
#5460=ORIENTED_EDGE('',*,*,#4020,.F.);
#5461=ORIENTED_EDGE('',*,*,#4023,.F.);
#5462=ORIENTED_EDGE('',*,*,#4026,.F.);
#5463=ORIENTED_EDGE('',*,*,#4027,.F.);
#5464=ORIENTED_EDGE('',*,*,#4028,.F.);
#5465=ORIENTED_EDGE('',*,*,#4029,.T.);
#5466=ORIENTED_EDGE('',*,*,#4027,.T.);
#5467=ORIENTED_EDGE('',*,*,#4029,.F.);
#5468=ORIENTED_EDGE('',*,*,#4030,.F.);
#5469=ORIENTED_EDGE('',*,*,#4031,.T.);
#5470=ORIENTED_EDGE('',*,*,#4028,.T.);
#5471=ORIENTED_EDGE('',*,*,#4031,.F.);
#5472=ORIENTED_EDGE('',*,*,#4032,.F.);
#5473=ORIENTED_EDGE('',*,*,#4033,.T.);
#5474=ORIENTED_EDGE('',*,*,#4030,.T.);
#5475=ORIENTED_EDGE('',*,*,#4033,.F.);
#5476=ORIENTED_EDGE('',*,*,#4032,.T.);
#5477=ORIENTED_EDGE('',*,*,#4034,.F.);
#5478=ORIENTED_EDGE('',*,*,#4035,.F.);
#5479=ORIENTED_EDGE('',*,*,#4036,.T.);
#5480=ORIENTED_EDGE('',*,*,#4034,.T.);
#5481=ORIENTED_EDGE('',*,*,#4036,.F.);
#5482=ORIENTED_EDGE('',*,*,#4026,.T.);
#5483=ORIENTED_EDGE('',*,*,#4037,.T.);
#5484=ORIENTED_EDGE('',*,*,#4035,.T.);
#5485=ORIENTED_EDGE('',*,*,#4037,.F.);
#5682=CYLINDRICAL_SURFACE('',#7305,0.35);
#5683=CYLINDRICAL_SURFACE('',#7313,0.1954);
#6035=ADVANCED_FACE('',(#1229),#867,.F.);
#6036=ADVANCED_FACE('',(#1230),#868,.F.);
#6037=ADVANCED_FACE('',(#1231),#869,.F.);
#6038=ADVANCED_FACE('',(#1232),#870,.F.);
#6039=ADVANCED_FACE('',(#1233),#871,.F.);
#6040=ADVANCED_FACE('',(#1234),#872,.F.);
#6041=ADVANCED_FACE('',(#1235),#873,.F.);
#6042=ADVANCED_FACE('',(#1236),#874,.F.);
#6043=ADVANCED_FACE('',(#1237),#875,.F.);
#6044=ADVANCED_FACE('',(#1238),#876,.T.);
#6045=ADVANCED_FACE('',(#1239),#307,.T.);
#6046=ADVANCED_FACE('',(#1240),#5682,.T.);
#6047=ADVANCED_FACE('',(#1241),#308,.T.);
#6048=ADVANCED_FACE('',(#1242,#683),#877,.T.);
#6049=ADVANCED_FACE('',(#1243),#309,.T.);
#6050=ADVANCED_FACE('',(#1244),#5683,.T.);
#6113=CLOSED_SHELL('',(#6035,#6036,#6037,#6038,#6039,#6040,#6041,#6042));
#6114=CLOSED_SHELL('',(#6043,#6044,#6045,#6046,#6047,#6048,#6049,#6050));
#7290=AXIS2_PLACEMENT_3D('',#11626,#9169,#9170);
#7291=AXIS2_PLACEMENT_3D('',#11627,#9171,#9172);
#7292=AXIS2_PLACEMENT_3D('',#11636,#9177,#9178);
#7293=AXIS2_PLACEMENT_3D('',#11642,#9182,#9183);
#7294=AXIS2_PLACEMENT_3D('',#11648,#9187,#9188);
#7295=AXIS2_PLACEMENT_3D('',#11654,#9192,#9193);
#7296=AXIS2_PLACEMENT_3D('',#11660,#9197,#9198);
#7297=AXIS2_PLACEMENT_3D('',#11663,#9201,#9202);
#7298=AXIS2_PLACEMENT_3D('',#11664,#9203,#9204);
#7299=AXIS2_PLACEMENT_3D('',#11665,#9205,#9206);
#7300=AXIS2_PLACEMENT_3D('',#11667,#9207,#9208);
#7301=AXIS2_PLACEMENT_3D('',#11668,#9209,#9210);
#7302=AXIS2_PLACEMENT_3D('',#11670,#9211,#9212);
#7303=AXIS2_PLACEMENT_3D('',#11671,#9213,#9214);
#7304=AXIS2_PLACEMENT_3D('',#11673,#9215,#9216);
#7305=AXIS2_PLACEMENT_3D('',#11675,#9218,#9219);
#7306=AXIS2_PLACEMENT_3D('',#11677,#9220,#9221);
#7307=AXIS2_PLACEMENT_3D('',#11679,#9223,#9224);
#7308=AXIS2_PLACEMENT_3D('',#11681,#9225,#9226);
#7309=AXIS2_PLACEMENT_3D('',#11683,#9228,#9229);
#7310=AXIS2_PLACEMENT_3D('',#11685,#9230,#9231);
#7311=AXIS2_PLACEMENT_3D('',#11686,#9232,#9233);
#7312=AXIS2_PLACEMENT_3D('',#11688,#9234,#9235);
#7313=AXIS2_PLACEMENT_3D('',#11690,#9237,#9238);
#9169=DIRECTION('axis',(0.,0.,1.));
#9170=DIRECTION('refdir',(1.,0.,0.));
#9171=DIRECTION('center_axis',(0.866025403784439,0.,-0.5));
#9172=DIRECTION('ref_axis',(0.5,0.,0.866025403784439));
#9173=DIRECTION('',(-0.5,0.,-0.866025403784439));
#9174=DIRECTION('',(0.,-1.,0.));
#9175=DIRECTION('',(0.5,0.,0.866025403784439));
#9176=DIRECTION('',(0.,-1.,0.));
#9177=DIRECTION('center_axis',(1.60246890531964E-16,0.,-1.));
#9178=DIRECTION('ref_axis',(1.,0.,1.60246890531964E-16));
#9179=DIRECTION('',(-1.,0.,-1.60246890531964E-16));
#9180=DIRECTION('',(0.,-1.,0.));
#9181=DIRECTION('',(1.,0.,1.60246890531964E-16));
#9182=DIRECTION('center_axis',(-0.866025403784439,0.,-0.5));
#9183=DIRECTION('ref_axis',(0.5,0.,-0.866025403784439));
#9184=DIRECTION('',(-0.5,0.,0.866025403784439));
#9185=DIRECTION('',(0.,-1.,0.));
#9186=DIRECTION('',(0.5,0.,-0.866025403784439));
#9187=DIRECTION('center_axis',(-0.866025403784439,0.,0.5));
#9188=DIRECTION('ref_axis',(-0.5,0.,-0.866025403784439));
#9189=DIRECTION('',(0.5,0.,0.866025403784439));
#9190=DIRECTION('',(0.,-1.,0.));
#9191=DIRECTION('',(-0.5,0.,-0.866025403784439));
#9192=DIRECTION('center_axis',(-1.60246890531964E-16,0.,1.));
#9193=DIRECTION('ref_axis',(-1.,0.,-1.60246890531964E-16));
#9194=DIRECTION('',(1.,0.,1.60246890531964E-16));
#9195=DIRECTION('',(0.,-1.,0.));
#9196=DIRECTION('',(-1.,0.,-1.60246890531964E-16));
#9197=DIRECTION('center_axis',(0.866025403784439,0.,0.5));
#9198=DIRECTION('ref_axis',(-0.5,0.,0.866025403784439));
#9199=DIRECTION('',(0.5,0.,-0.866025403784439));
#9200=DIRECTION('',(-0.5,0.,0.866025403784439));
#9201=DIRECTION('center_axis',(0.,1.,0.));
#9202=DIRECTION('ref_axis',(1.,0.,0.));
#9203=DIRECTION('center_axis',(0.,-1.,0.));
#9204=DIRECTION('ref_axis',(0.,0.,-1.));
#9205=DIRECTION('center_axis',(0.,1.,0.));
#9206=DIRECTION('ref_axis',(1.,0.,0.));
#9207=DIRECTION('center_axis',(0.,1.,0.));
#9208=DIRECTION('ref_axis',(1.,0.,0.));
#9209=DIRECTION('center_axis',(0.,1.,0.));
#9210=DIRECTION('ref_axis',(0.,0.,1.));
#9211=DIRECTION('center_axis',(0.,-1.,0.));
#9212=DIRECTION('ref_axis',(1.,0.,0.));
#9213=DIRECTION('center_axis',(0.,-1.,0.));
#9214=DIRECTION('ref_axis',(1.,0.,0.));
#9215=DIRECTION('center_axis',(0.,-1.,0.));
#9216=DIRECTION('ref_axis',(1.,0.,0.));
#9217=DIRECTION('',(0.707106781186547,0.707106781186548,8.65956056235493E-17));
#9218=DIRECTION('center_axis',(0.,-1.,0.));
#9219=DIRECTION('ref_axis',(1.,0.,0.));
#9220=DIRECTION('center_axis',(0.,-1.,0.));
#9221=DIRECTION('ref_axis',(1.,0.,0.));
#9222=DIRECTION('',(0.,1.,0.));
#9223=DIRECTION('center_axis',(0.,1.,0.));
#9224=DIRECTION('ref_axis',(1.,0.,0.));
#9225=DIRECTION('center_axis',(0.,-1.,0.));
#9226=DIRECTION('ref_axis',(1.,0.,0.));
#9227=DIRECTION('',(-0.707106781186547,0.707106781186548,-8.65956056235493E-17));
#9228=DIRECTION('center_axis',(0.,-1.,0.));
#9229=DIRECTION('ref_axis',(0.,0.,-1.));
#9230=DIRECTION('center_axis',(0.,-1.,0.));
#9231=DIRECTION('ref_axis',(1.,0.,0.));
#9232=DIRECTION('center_axis',(0.,1.,0.));
#9233=DIRECTION('ref_axis',(1.,0.,0.));
#9234=DIRECTION('center_axis',(0.,1.,0.));
#9235=DIRECTION('ref_axis',(1.,0.,0.));
#9236=DIRECTION('',(-0.447213595499958,0.894427190999916,-5.47678698264203E-17));
#9237=DIRECTION('center_axis',(0.,-1.,0.));
#9238=DIRECTION('ref_axis',(1.,0.,0.));
#9239=DIRECTION('',(0.,1.,0.));
#11626=CARTESIAN_POINT('',(0.,0.,0.));
#11627=CARTESIAN_POINT('Origin',(0.0866025403784439,-0.4,-0.15));
#11628=CARTESIAN_POINT('',(0.173205080756888,-0.4,0.));
#11629=CARTESIAN_POINT('',(0.0866025403784439,-0.4,-0.15));
#11630=CARTESIAN_POINT('',(0.173205080756888,-0.4,0.));
#11631=CARTESIAN_POINT('',(0.0866025403784439,-0.64,-0.15));
#11632=CARTESIAN_POINT('',(0.0866025403784439,-0.4,-0.15));
#11633=CARTESIAN_POINT('',(0.173205080756888,-0.64,0.));
#11634=CARTESIAN_POINT('',(0.173205080756888,-0.64,0.));
#11635=CARTESIAN_POINT('',(0.173205080756888,-0.4,0.));
#11636=CARTESIAN_POINT('Origin',(-0.0866025403784438,-0.4,-0.15));
#11637=CARTESIAN_POINT('',(-0.0866025403784438,-0.4,-0.15));
#11638=CARTESIAN_POINT('',(0.0866025403784439,-0.4,-0.15));
#11639=CARTESIAN_POINT('',(-0.0866025403784438,-0.64,-0.15));
#11640=CARTESIAN_POINT('',(-0.0866025403784438,-0.4,-0.15));
#11641=CARTESIAN_POINT('',(0.0866025403784439,-0.64,-0.15));
#11642=CARTESIAN_POINT('Origin',(-0.173205080756888,-0.4,-2.77555756156289E-17));
#11643=CARTESIAN_POINT('',(-0.173205080756888,-0.4,-2.12115047744981E-17));
#11644=CARTESIAN_POINT('',(-0.0866025403784438,-0.4,-0.15));
#11645=CARTESIAN_POINT('',(-0.173205080756888,-0.64,-2.77555756156289E-17));
#11646=CARTESIAN_POINT('',(-0.173205080756888,-0.4,-2.12115047744981E-17));
#11647=CARTESIAN_POINT('',(-0.0866025403784438,-0.64,-0.15));
#11648=CARTESIAN_POINT('Origin',(-0.0866025403784439,-0.4,0.15));
#11649=CARTESIAN_POINT('',(-0.0866025403784439,-0.4,0.15));
#11650=CARTESIAN_POINT('',(-0.173205080756888,-0.4,-2.12115047744981E-17));
#11651=CARTESIAN_POINT('',(-0.0866025403784439,-0.64,0.15));
#11652=CARTESIAN_POINT('',(-0.0866025403784439,-0.4,0.15));
#11653=CARTESIAN_POINT('',(-0.173205080756888,-0.64,-2.12115047744981E-17));
#11654=CARTESIAN_POINT('Origin',(0.0866025403784439,-0.4,0.15));
#11655=CARTESIAN_POINT('',(0.0866025403784439,-0.4,0.15));
#11656=CARTESIAN_POINT('',(-0.0866025403784439,-0.4,0.15));
#11657=CARTESIAN_POINT('',(0.0866025403784439,-0.64,0.15));
#11658=CARTESIAN_POINT('',(0.0866025403784439,-0.4,0.15));
#11659=CARTESIAN_POINT('',(-0.0866025403784439,-0.64,0.15));
#11660=CARTESIAN_POINT('Origin',(0.173205080756888,-0.4,0.));
#11661=CARTESIAN_POINT('',(0.0866025403784439,-0.4,0.15));
#11662=CARTESIAN_POINT('',(0.0866025403784439,-0.64,0.15));
#11663=CARTESIAN_POINT('Origin',(0.,-0.4,-2.77555756156289E-17));
#11664=CARTESIAN_POINT('Origin',(0.,-0.64,-2.77555756156289E-17));
#11665=CARTESIAN_POINT('Origin',(0.,-1.,0.));
#11666=CARTESIAN_POINT('',(-0.1954,-1.,2.39295984553393E-17));
#11667=CARTESIAN_POINT('Origin',(0.,-1.,0.));
#11668=CARTESIAN_POINT('Origin',(0.3,0.4,0.));
#11669=CARTESIAN_POINT('',(-0.3,0.4,-3.67394039744206E-17));
#11670=CARTESIAN_POINT('Origin',(0.,0.4,0.));
#11671=CARTESIAN_POINT('Origin',(0.,0.375,0.));
#11672=CARTESIAN_POINT('',(-0.35,0.35,-4.28626379701573E-17));
#11673=CARTESIAN_POINT('Origin',(0.,0.35,0.));
#11674=CARTESIAN_POINT('',(-0.325,0.375,-3.9801020972289E-17));
#11675=CARTESIAN_POINT('Origin',(0.,0.19,0.));
#11676=CARTESIAN_POINT('',(-0.35,0.03,-4.28626379701574E-17));
#11677=CARTESIAN_POINT('Origin',(0.,0.03,0.));
#11678=CARTESIAN_POINT('',(-0.35,0.19,-4.28626379701574E-17));
#11679=CARTESIAN_POINT('Origin',(0.,0.0149999999999999,0.));
#11680=CARTESIAN_POINT('',(-0.32,-3.29597460435593E-17,-3.91886975727153E-17));
#11681=CARTESIAN_POINT('Origin',(0.,0.,0.));
#11682=CARTESIAN_POINT('',(-0.335,0.0149999999999999,-4.10256677714363E-17));
#11683=CARTESIAN_POINT('Origin',(0.22,0.,0.));
#11684=CARTESIAN_POINT('',(-0.22,-6.93889390390723E-18,-2.69422295812418E-17));
#11685=CARTESIAN_POINT('Origin',(0.,0.,0.));
#11686=CARTESIAN_POINT('Origin',(0.,-0.02,0.));
#11687=CARTESIAN_POINT('',(-0.1954,-0.0492,2.39295984553393E-17));
#11688=CARTESIAN_POINT('Origin',(0.,-0.0492,0.));
#11689=CARTESIAN_POINT('',(-0.21,-0.02,-2.57175827820944E-17));
#11690=CARTESIAN_POINT('Origin',(0.,-0.8,0.));
#11691=CARTESIAN_POINT('',(-0.1954,-0.8,-2.39295984553393E-17));
#11864=UNCERTAINTY_MEASURE_WITH_UNIT(LENGTH_MEASURE(0.001),#11917,
'DISTANCE_ACCURACY_VALUE',
'Maximum model space distance between geometric entities at asserted c
onnectivities');
#11869=UNCERTAINTY_MEASURE_WITH_UNIT(LENGTH_MEASURE(0.001),#11917,
'DISTANCE_ACCURACY_VALUE',
'Maximum model space distance between geometric entities at asserted c
onnectivities');
#11911=(
GEOMETRIC_REPRESENTATION_CONTEXT(3)
GLOBAL_UNCERTAINTY_ASSIGNED_CONTEXT((#11864))
GLOBAL_UNIT_ASSIGNED_CONTEXT((#11917,#11919,#11920))
REPRESENTATION_CONTEXT('','3D')
);
#11916=(
GEOMETRIC_REPRESENTATION_CONTEXT(3)
GLOBAL_UNCERTAINTY_ASSIGNED_CONTEXT((#11869))
GLOBAL_UNIT_ASSIGNED_CONTEXT((#11917,#11919,#11920))
REPRESENTATION_CONTEXT('','3D')
);
#11917=(
LENGTH_UNIT()
NAMED_UNIT(*)
SI_UNIT(.CENTI.,.METRE.)
);
#11919=(
NAMED_UNIT(*)
PLANE_ANGLE_UNIT()
SI_UNIT($,.RADIAN.)
);
#11920=(
NAMED_UNIT(*)
SI_UNIT($,.STERADIAN.)
SOLID_ANGLE_UNIT()
);
#11962=SHAPE_DEFINITION_REPRESENTATION(#12013,#12120);
#12013=PRODUCT_DEFINITION_SHAPE('',$,#12167);
#12120=SHAPE_REPRESENTATION('',(#7290),#11911);
#12125=PRODUCT_DEFINITION_CONTEXT('part definition',#12265,'design');
#12167=PRODUCT_DEFINITION('M4x10 Cap Screw','M4x10 Cap Screw',#12213,#12125);
#12213=PRODUCT_DEFINITION_FORMATION('',$,#12308);
#12265=APPLICATION_CONTEXT(
'Core Data for Automotive Mechanical Design Process');
#12266=PRODUCT_CONTEXT('part definition',#12265,'mechanical');
#12308=PRODUCT('M4x10 Cap Screw','M4x10 Cap Screw','M4x10 Cap Screw',(#12266));
#12376=COLOUR_RGB('Black',0.12,0.14,0.17);
#12377=FILL_AREA_STYLE_COLOUR('',#12376);
#12378=FILL_AREA_STYLE('',(#12377));
#12379=SURFACE_STYLE_FILL_AREA(#12378);
#12380=SURFACE_SIDE_STYLE('',(#12379));
#12381=SURFACE_STYLE_USAGE(.BOTH.,#12380);
#12382=PRESENTATION_STYLE_ASSIGNMENT((#12381));
ENDSEC;
END-ISO-10303-21;
